ISO-10303-21;
HEADER;
/* Generated by software containing ST-Developer
 * from STEP Tools, Inc. (www.steptools.com) 
 */

FILE_DESCRIPTION(
/* description */ ('PAT-001'),
/* implementation_level */ '2;1');

FILE_NAME(
/* name */ 'Hex Bolt - M8x40.step',
/* time_stamp */ '2026-10-29T17:07:15-07:00',
/* author */ (''),
/* organization */ (''),
/* preprocessor_version */ 'ST-DEVELOPER v20.2',
/* originating_system */ 'Autodesk Translation Framework v15.17.0.0',
/* authorisation */ '');

FILE_SCHEMA (('AUTOMOTIVE_DESIGN { 1 0 10303 214 3 1 1 }'));
ENDSEC;

DATA;
#10=MECHANICAL_DESIGN_GEOMETRIC_PRESENTATION_REPRESENTATION('',(#399),#9622);
#11=(
BOUNDED_CURVE()
B_SPLINE_CURVE(2,(#9167,#9168,#9169),.UNSPECIFIED.,.F.,.F.)
B_SPLINE_CURVE_WITH_KNOTS((3,3),(0.14973948338295,0.97160236658079),
 .UNSPECIFIED.)
CURVE()
GEOMETRIC_REPRESENTATION_ITEM()
RATIONAL_B_SPLINE_CURVE((1.07140024848292,1.23714644374248,1.07140024848292))
REPRESENTATION_ITEM('')
);
#12=(
BOUNDED_CURVE()
B_SPLINE_CURVE(2,(#9171,#9172,#9173),.UNSPECIFIED.,.F.,.F.)
B_SPLINE_CURVE_WITH_KNOTS((3,3),(0.14973948338295,0.97160236658079),
 .UNSPECIFIED.)
CURVE()
GEOMETRIC_REPRESENTATION_ITEM()
RATIONAL_B_SPLINE_CURVE((1.07140024848292,1.23714644374248,1.07140024848292))
REPRESENTATION_ITEM('')
);
#13=(
BOUNDED_CURVE()
B_SPLINE_CURVE(2,(#9175,#9176,#9177),.UNSPECIFIED.,.F.,.F.)
B_SPLINE_CURVE_WITH_KNOTS((3,3),(0.14973948338295,0.97160236658079),
 .UNSPECIFIED.)
CURVE()
GEOMETRIC_REPRESENTATION_ITEM()
RATIONAL_B_SPLINE_CURVE((1.07140024848292,1.23714644374248,1.07140024848292))
REPRESENTATION_ITEM('')
);
#14=(
BOUNDED_CURVE()
B_SPLINE_CURVE(2,(#9179,#9180,#9181),.UNSPECIFIED.,.F.,.F.)
B_SPLINE_CURVE_WITH_KNOTS((3,3),(0.149739483382949,0.971602366580789),
 .UNSPECIFIED.)
CURVE()
GEOMETRIC_REPRESENTATION_ITEM()
RATIONAL_B_SPLINE_CURVE((1.07140024848292,1.23714644374248,1.07140024848292))
REPRESENTATION_ITEM('')
);
#15=(
BOUNDED_CURVE()
B_SPLINE_CURVE(2,(#9183,#9184,#9185),.UNSPECIFIED.,.F.,.F.)
B_SPLINE_CURVE_WITH_KNOTS((3,3),(0.14973948338295,0.971602366580789),
 .UNSPECIFIED.)
CURVE()
GEOMETRIC_REPRESENTATION_ITEM()
RATIONAL_B_SPLINE_CURVE((1.07140024848292,1.23714644374248,1.07140024848292))
REPRESENTATION_ITEM('')
);
#16=(
BOUNDED_CURVE()
B_SPLINE_CURVE(2,(#9186,#9187,#9188),.UNSPECIFIED.,.F.,.F.)
B_SPLINE_CURVE_WITH_KNOTS((3,3),(0.14973948338295,0.97160236658079),
 .UNSPECIFIED.)
CURVE()
GEOMETRIC_REPRESENTATION_ITEM()
RATIONAL_B_SPLINE_CURVE((1.07140024848292,1.23714644374248,1.07140024848292))
REPRESENTATION_ITEM('')
);
#313=CONICAL_SURFACE('',#5917,0.36,0.785398163397451);
#314=CONICAL_SURFACE('',#5920,0.734027674973257,1.0471975511966);
#341=SHAPE_REPRESENTATION_RELATIONSHIP('SRR','None',#9765,#366);
#366=ADVANCED_BREP_SHAPE_REPRESENTATION('',(#431),#9614);
#399=STYLED_ITEM('',(#9969),#431);
#431=MANIFOLD_SOLID_BREP('Body1',#5225);
#490=FACE_BOUND('',#1300,.T.);
#677=PLANE('',#5919);
#678=PLANE('',#5922);
#679=PLANE('',#5923);
#680=PLANE('',#5924);
#681=PLANE('',#5925);
#682=PLANE('',#5926);
#683=PLANE('',#5927);
#684=PLANE('',#5928);
#685=PLANE('',#5929);
#939=FACE_OUTER_BOUND('',#1288,.T.);
#940=FACE_OUTER_BOUND('',#1289,.T.);
#941=FACE_OUTER_BOUND('',#1290,.T.);
#942=FACE_OUTER_BOUND('',#1291,.T.);
#943=FACE_OUTER_BOUND('',#1292,.T.);
#944=FACE_OUTER_BOUND('',#1293,.T.);
#945=FACE_OUTER_BOUND('',#1294,.T.);
#946=FACE_OUTER_BOUND('',#1295,.T.);
#947=FACE_OUTER_BOUND('',#1296,.T.);
#948=FACE_OUTER_BOUND('',#1297,.T.);
#949=FACE_OUTER_BOUND('',#1298,.T.);
#950=FACE_OUTER_BOUND('',#1299,.T.);
#1288=EDGE_LOOP('',(#4531,#4532,#4533,#4534));
#1289=EDGE_LOOP('',(#4535,#4536,#4537,#4538));
#1290=EDGE_LOOP('',(#4539));
#1291=EDGE_LOOP('',(#4540,#4541,#4542,#4543,#4544,#4545,#4546,#4547,#4548));
#1292=EDGE_LOOP('',(#4549,#4550,#4551,#4552));
#1293=EDGE_LOOP('',(#4553,#4554,#4555,#4556));
#1294=EDGE_LOOP('',(#4557,#4558,#4559,#4560));
#1295=EDGE_LOOP('',(#4561,#4562,#4563,#4564));
#1296=EDGE_LOOP('',(#4565,#4566,#4567,#4568));
#1297=EDGE_LOOP('',(#4569,#4570,#4571,#4572));
#1298=EDGE_LOOP('',(#4573));
#1299=EDGE_LOOP('',(#4574,#4575,#4576,#4577,#4578,#4579));
#1300=EDGE_LOOP('',(#4580));
#1733=LINE('',#9154,#2138);
#1734=LINE('',#9159,#2139);
#1735=LINE('',#9165,#2140);
#1736=LINE('',#9191,#2141);
#1737=LINE('',#9193,#2142);
#1738=LINE('',#9194,#2143);
#1739=LINE('',#9197,#2144);
#1740=LINE('',#9198,#2145);
#1741=LINE('',#9201,#2146);
#1742=LINE('',#9202,#2147);
#1743=LINE('',#9205,#2148);
#1744=LINE('',#9206,#2149);
#1745=LINE('',#9209,#2150);
#1746=LINE('',#9210,#2151);
#1747=LINE('',#9212,#2152);
#2138=VECTOR('',#7256,0.4);
#2139=VECTOR('',#7263,0.36);
#2140=VECTOR('',#7270,0.734027674973257);
#2141=VECTOR('',#7273,1.);
#2142=VECTOR('',#7274,1.);
#2143=VECTOR('',#7275,1.);
#2144=VECTOR('',#7278,1.);
#2145=VECTOR('',#7279,1.);
#2146=VECTOR('',#7282,1.);
#2147=VECTOR('',#7283,1.);
#2148=VECTOR('',#7286,1.);
#2149=VECTOR('',#7287,1.);
#2150=VECTOR('',#7290,1.);
#2151=VECTOR('',#7291,1.);
#2152=VECTOR('',#7294,1.);
#2360=CIRCLE('',#5915,0.3933);
#2361=CIRCLE('',#5916,0.3933);
#2362=CIRCLE('',#5918,0.32);
#2363=CIRCLE('',#5921,0.6175);
#2766=VERTEX_POINT('',#9151);
#2767=VERTEX_POINT('',#9153);
#2768=VERTEX_POINT('',#9157);
#2769=VERTEX_POINT('',#9162);
#2770=VERTEX_POINT('',#9164);
#2771=VERTEX_POINT('',#9166);
#2772=VERTEX_POINT('',#9170);
#2773=VERTEX_POINT('',#9174);
#2774=VERTEX_POINT('',#9178);
#2775=VERTEX_POINT('',#9182);
#2776=VERTEX_POINT('',#9190);
#2777=VERTEX_POINT('',#9192);
#2778=VERTEX_POINT('',#9196);
#2779=VERTEX_POINT('',#9200);
#2780=VERTEX_POINT('',#9204);
#2781=VERTEX_POINT('',#9208);
#3369=EDGE_CURVE('',#2766,#2766,#2360,.F.);
#3370=EDGE_CURVE('',#2766,#2767,#1733,.T.);
#3371=EDGE_CURVE('',#2767,#2767,#2361,.F.);
#3372=EDGE_CURVE('',#2768,#2768,#2362,.T.);
#3373=EDGE_CURVE('',#2768,#2766,#1734,.T.);
#3374=EDGE_CURVE('',#2769,#2769,#2363,.T.);
#3375=EDGE_CURVE('',#2769,#2770,#1735,.T.);
#3376=EDGE_CURVE('',#2771,#2770,#11,.T.);
#3377=EDGE_CURVE('',#2772,#2771,#12,.T.);
#3378=EDGE_CURVE('',#2773,#2772,#13,.T.);
#3379=EDGE_CURVE('',#2774,#2773,#14,.T.);
#3380=EDGE_CURVE('',#2775,#2774,#15,.T.);
#3381=EDGE_CURVE('',#2770,#2775,#16,.T.);
#3382=EDGE_CURVE('',#2776,#2774,#1736,.T.);
#3383=EDGE_CURVE('',#2776,#2777,#1737,.T.);
#3384=EDGE_CURVE('',#2777,#2775,#1738,.T.);
#3385=EDGE_CURVE('',#2778,#2773,#1739,.T.);
#3386=EDGE_CURVE('',#2778,#2776,#1740,.T.);
#3387=EDGE_CURVE('',#2779,#2772,#1741,.T.);
#3388=EDGE_CURVE('',#2779,#2778,#1742,.T.);
#3389=EDGE_CURVE('',#2780,#2771,#1743,.T.);
#3390=EDGE_CURVE('',#2780,#2779,#1744,.T.);
#3391=EDGE_CURVE('',#2781,#2770,#1745,.T.);
#3392=EDGE_CURVE('',#2781,#2780,#1746,.T.);
#3393=EDGE_CURVE('',#2777,#2781,#1747,.T.);
#4531=ORIENTED_EDGE('',*,*,#3369,.F.);
#4532=ORIENTED_EDGE('',*,*,#3370,.T.);
#4533=ORIENTED_EDGE('',*,*,#3371,.F.);
#4534=ORIENTED_EDGE('',*,*,#3370,.F.);
#4535=ORIENTED_EDGE('',*,*,#3372,.F.);
#4536=ORIENTED_EDGE('',*,*,#3373,.T.);
#4537=ORIENTED_EDGE('',*,*,#3369,.T.);
#4538=ORIENTED_EDGE('',*,*,#3373,.F.);
#4539=ORIENTED_EDGE('',*,*,#3372,.T.);
#4540=ORIENTED_EDGE('',*,*,#3374,.F.);
#4541=ORIENTED_EDGE('',*,*,#3375,.T.);
#4542=ORIENTED_EDGE('',*,*,#3376,.F.);
#4543=ORIENTED_EDGE('',*,*,#3377,.F.);
#4544=ORIENTED_EDGE('',*,*,#3378,.F.);
#4545=ORIENTED_EDGE('',*,*,#3379,.F.);
#4546=ORIENTED_EDGE('',*,*,#3380,.F.);
#4547=ORIENTED_EDGE('',*,*,#3381,.F.);
#4548=ORIENTED_EDGE('',*,*,#3375,.F.);
#4549=ORIENTED_EDGE('',*,*,#3380,.T.);
#4550=ORIENTED_EDGE('',*,*,#3382,.F.);
#4551=ORIENTED_EDGE('',*,*,#3383,.T.);
#4552=ORIENTED_EDGE('',*,*,#3384,.T.);
#4553=ORIENTED_EDGE('',*,*,#3379,.T.);
#4554=ORIENTED_EDGE('',*,*,#3385,.F.);
#4555=ORIENTED_EDGE('',*,*,#3386,.T.);
#4556=ORIENTED_EDGE('',*,*,#3382,.T.);
#4557=ORIENTED_EDGE('',*,*,#3378,.T.);
#4558=ORIENTED_EDGE('',*,*,#3387,.F.);
#4559=ORIENTED_EDGE('',*,*,#3388,.T.);
#4560=ORIENTED_EDGE('',*,*,#3385,.T.);
#4561=ORIENTED_EDGE('',*,*,#3377,.T.);
#4562=ORIENTED_EDGE('',*,*,#3389,.F.);
#4563=ORIENTED_EDGE('',*,*,#3390,.T.);
#4564=ORIENTED_EDGE('',*,*,#3387,.T.);
#4565=ORIENTED_EDGE('',*,*,#3376,.T.);
#4566=ORIENTED_EDGE('',*,*,#3391,.F.);
#4567=ORIENTED_EDGE('',*,*,#3392,.T.);
#4568=ORIENTED_EDGE('',*,*,#3389,.T.);
#4569=ORIENTED_EDGE('',*,*,#3381,.T.);
#4570=ORIENTED_EDGE('',*,*,#3384,.F.);
#4571=ORIENTED_EDGE('',*,*,#3393,.T.);
#4572=ORIENTED_EDGE('',*,*,#3391,.T.);
#4573=ORIENTED_EDGE('',*,*,#3374,.T.);
#4574=ORIENTED_EDGE('',*,*,#3388,.F.);
#4575=ORIENTED_EDGE('',*,*,#3390,.F.);
#4576=ORIENTED_EDGE('',*,*,#3392,.F.);
#4577=ORIENTED_EDGE('',*,*,#3393,.F.);
#4578=ORIENTED_EDGE('',*,*,#3383,.F.);
#4579=ORIENTED_EDGE('',*,*,#3386,.F.);
#4580=ORIENTED_EDGE('',*,*,#3371,.T.);
#4876=CYLINDRICAL_SURFACE('',#5914,0.3933);
#5126=ADVANCED_FACE('',(#939),#4876,.T.);
#5127=ADVANCED_FACE('',(#940),#313,.T.);
#5128=ADVANCED_FACE('',(#941),#677,.T.);
#5129=ADVANCED_FACE('',(#942),#314,.T.);
#5130=ADVANCED_FACE('',(#943),#678,.T.);
#5131=ADVANCED_FACE('',(#944),#679,.T.);
#5132=ADVANCED_FACE('',(#945),#680,.T.);
#5133=ADVANCED_FACE('',(#946),#681,.T.);
#5134=ADVANCED_FACE('',(#947),#682,.T.);
#5135=ADVANCED_FACE('',(#948),#683,.T.);
#5136=ADVANCED_FACE('',(#949),#684,.T.);
#5137=ADVANCED_FACE('',(#950,#490),#685,.F.);
#5225=CLOSED_SHELL('',(#5126,#5127,#5128,#5129,#5130,#5131,#5132,#5133,
#5134,#5135,#5136,#5137));
#5913=AXIS2_PLACEMENT_3D('',#9149,#7250,#7251);
#5914=AXIS2_PLACEMENT_3D('',#9150,#7252,#7253);
#5915=AXIS2_PLACEMENT_3D('',#9152,#7254,#7255);
#5916=AXIS2_PLACEMENT_3D('',#9155,#7257,#7258);
#5917=AXIS2_PLACEMENT_3D('',#9156,#7259,#7260);
#5918=AXIS2_PLACEMENT_3D('',#9158,#7261,#7262);
#5919=AXIS2_PLACEMENT_3D('',#9160,#7264,#7265);
#5920=AXIS2_PLACEMENT_3D('',#9161,#7266,#7267);
#5921=AXIS2_PLACEMENT_3D('',#9163,#7268,#7269);
#5922=AXIS2_PLACEMENT_3D('',#9189,#7271,#7272);
#5923=AXIS2_PLACEMENT_3D('',#9195,#7276,#7277);
#5924=AXIS2_PLACEMENT_3D('',#9199,#7280,#7281);
#5925=AXIS2_PLACEMENT_3D('',#9203,#7284,#7285);
#5926=AXIS2_PLACEMENT_3D('',#9207,#7288,#7289);
#5927=AXIS2_PLACEMENT_3D('',#9211,#7292,#7293);
#5928=AXIS2_PLACEMENT_3D('',#9213,#7295,#7296);
#5929=AXIS2_PLACEMENT_3D('',#9214,#7297,#7298);
#7250=DIRECTION('axis',(0.,0.,1.));
#7251=DIRECTION('refdir',(1.,0.,0.));
#7252=DIRECTION('center_axis',(0.,-1.,0.));
#7253=DIRECTION('ref_axis',(1.,0.,0.));
#7254=DIRECTION('center_axis',(0.,1.,0.));
#7255=DIRECTION('ref_axis',(1.,0.,0.));
#7256=DIRECTION('',(0.,1.,0.));
#7257=DIRECTION('center_axis',(0.,-1.,0.));
#7258=DIRECTION('ref_axis',(1.,0.,0.));
#7259=DIRECTION('center_axis',(0.,1.,0.));
#7260=DIRECTION('ref_axis',(1.,0.,0.));
#7261=DIRECTION('center_axis',(0.,-1.,0.));
#7262=DIRECTION('ref_axis',(1.,0.,0.));
#7263=DIRECTION('',(-0.707106781186549,0.707106781186546,-8.65956056235496E-17));
#7264=DIRECTION('center_axis',(0.,-1.,0.));
#7265=DIRECTION('ref_axis',(0.,0.,-1.));
#7266=DIRECTION('center_axis',(0.,-1.,0.));
#7267=DIRECTION('ref_axis',(1.,0.,0.));
#7268=DIRECTION('center_axis',(0.,1.,0.));
#7269=DIRECTION('ref_axis',(1.,0.,0.));
#7270=DIRECTION('',(-0.866025403784439,-0.5,-1.06057523872491E-16));
#7271=DIRECTION('center_axis',(1.4792020664489E-16,0.,-1.));
#7272=DIRECTION('ref_axis',(-1.,0.,-1.4792020664489E-16));
#7273=DIRECTION('',(0.,1.,0.));
#7274=DIRECTION('',(-1.,0.,-1.4792020664489E-16));
#7275=DIRECTION('',(0.,1.,0.));
#7276=DIRECTION('center_axis',(0.866025403784439,0.,-0.5));
#7277=DIRECTION('ref_axis',(-0.5,0.,-0.866025403784439));
#7278=DIRECTION('',(0.,1.,0.));
#7279=DIRECTION('',(-0.5,0.,-0.866025403784439));
#7280=DIRECTION('center_axis',(0.866025403784439,0.,0.5));
#7281=DIRECTION('ref_axis',(0.5,0.,-0.866025403784439));
#7282=DIRECTION('',(0.,1.,0.));
#7283=DIRECTION('',(0.5,0.,-0.866025403784439));
#7284=DIRECTION('center_axis',(-2.95840413289779E-16,0.,1.));
#7285=DIRECTION('ref_axis',(1.,0.,2.95840413289779E-16));
#7286=DIRECTION('',(0.,1.,0.));
#7287=DIRECTION('',(1.,0.,2.95840413289779E-16));
#7288=DIRECTION('center_axis',(-0.866025403784439,0.,0.5));
#7289=DIRECTION('ref_axis',(0.5,0.,0.866025403784439));
#7290=DIRECTION('',(0.,1.,0.));
#7291=DIRECTION('',(0.5,0.,0.866025403784439));
#7292=DIRECTION('center_axis',(-0.866025403784439,0.,-0.5));
#7293=DIRECTION('ref_axis',(-0.5,0.,0.866025403784439));
#7294=DIRECTION('',(-0.5,0.,0.866025403784439));
#7295=DIRECTION('center_axis',(0.,1.,0.));
#7296=DIRECTION('ref_axis',(0.,0.,1.));
#7297=DIRECTION('center_axis',(0.,1.,0.));
#7298=DIRECTION('ref_axis',(1.,0.,0.));
#9149=CARTESIAN_POINT('',(0.,0.,0.));
#9150=CARTESIAN_POINT('Origin',(0.,-1.935,0.));
#9151=CARTESIAN_POINT('',(-0.3933,-3.9267,4.81653586104654E-17));
#9152=CARTESIAN_POINT('Origin',(0.,-3.9267,0.));
#9153=CARTESIAN_POINT('',(-0.3933,0.,-4.81653586104654E-17));
#9154=CARTESIAN_POINT('',(-0.3933,-1.935,-4.81653586104654E-17));
#9155=CARTESIAN_POINT('Origin',(0.,0.,0.));
#9156=CARTESIAN_POINT('Origin',(0.,-3.96,0.));
#9157=CARTESIAN_POINT('',(-0.32,-4.,-3.91886975727153E-17));
#9158=CARTESIAN_POINT('Origin',(0.,-4.,0.));
#9159=CARTESIAN_POINT('',(-0.36,-3.96,-4.40872847693047E-17));
#9160=CARTESIAN_POINT('Origin',(0.,-4.,0.));
#9161=CARTESIAN_POINT('Origin',(0.,0.462722715486149,0.));
#9162=CARTESIAN_POINT('',(-0.6175,0.53,-7.5621939847349E-17));
#9163=CARTESIAN_POINT('Origin',(0.,0.53,0.));
#9164=CARTESIAN_POINT('',(-0.750555349946514,0.453180457891261,-9.19165206894919E-17));
#9165=CARTESIAN_POINT('',(-0.734027674973257,0.462722715486149,-8.98924642641573E-17));
#9166=CARTESIAN_POINT('',(-0.375277674973257,0.453180457891261,0.65));
#9167=CARTESIAN_POINT('Ctrl Pts',(-0.375277674973257,0.45318045789126,0.65));
#9168=CARTESIAN_POINT('Ctrl Pts',(-0.562916512459968,0.561513791224244,
0.324999999999856));
#9169=CARTESIAN_POINT('Ctrl Pts',(-0.750555349946514,0.45318045789126,-9.19165206894919E-17));
#9170=CARTESIAN_POINT('',(0.375277674973257,0.453180457891261,0.65));
#9171=CARTESIAN_POINT('Ctrl Pts',(0.375277674973257,0.453180457891261,0.65));
#9172=CARTESIAN_POINT('Ctrl Pts',(-1.66922031752392E-13,0.561513791224244,
0.65));
#9173=CARTESIAN_POINT('Ctrl Pts',(-0.375277674973257,0.45318045789126,0.65));
#9174=CARTESIAN_POINT('',(0.750555349946514,0.453180457891261,0.));
#9175=CARTESIAN_POINT('Ctrl Pts',(0.750555349946514,0.453180457891261,0.));
#9176=CARTESIAN_POINT('Ctrl Pts',(0.562916512459802,0.561513791224244,0.325000000000144));
#9177=CARTESIAN_POINT('Ctrl Pts',(0.375277674973257,0.45318045789126,0.65));
#9178=CARTESIAN_POINT('',(0.375277674973257,0.453180457891261,-0.65));
#9179=CARTESIAN_POINT('Ctrl Pts',(0.375277674973257,0.45318045789126,-0.65));
#9180=CARTESIAN_POINT('Ctrl Pts',(0.562916512459968,0.561513791224244,-0.324999999999855));
#9181=CARTESIAN_POINT('Ctrl Pts',(0.750555349946514,0.453180457891261,0.));
#9182=CARTESIAN_POINT('',(-0.375277674973257,0.45318045789126,-0.65));
#9183=CARTESIAN_POINT('Ctrl Pts',(-0.375277674973257,0.453180457891261,
-0.65));
#9184=CARTESIAN_POINT('Ctrl Pts',(1.66866520601161E-13,0.561513791224244,
-0.65));
#9185=CARTESIAN_POINT('Ctrl Pts',(0.375277674973257,0.45318045789126,-0.65));
#9186=CARTESIAN_POINT('Ctrl Pts',(-0.750555349946514,0.453180457891261,
-9.19165206894919E-17));
#9187=CARTESIAN_POINT('Ctrl Pts',(-0.562916512459802,0.561513791224244,
-0.325000000000144));
#9188=CARTESIAN_POINT('Ctrl Pts',(-0.375277674973257,0.45318045789126,-0.65));
#9189=CARTESIAN_POINT('Origin',(0.375277674973257,0.,-0.65));
#9190=CARTESIAN_POINT('',(0.375277674973257,0.,-0.65));
#9191=CARTESIAN_POINT('',(0.375277674973257,0.,-0.65));
#9192=CARTESIAN_POINT('',(-0.375277674973257,0.,-0.65));
#9193=CARTESIAN_POINT('',(0.375277674973257,0.,-0.65));
#9194=CARTESIAN_POINT('',(-0.375277674973257,0.,-0.65));
#9195=CARTESIAN_POINT('Origin',(0.750555349946514,0.,0.));
#9196=CARTESIAN_POINT('',(0.750555349946514,0.,0.));
#9197=CARTESIAN_POINT('',(0.750555349946514,0.,0.));
#9198=CARTESIAN_POINT('',(0.750555349946514,0.,0.));
#9199=CARTESIAN_POINT('Origin',(0.375277674973257,0.,0.65));
#9200=CARTESIAN_POINT('',(0.375277674973257,0.,0.65));
#9201=CARTESIAN_POINT('',(0.375277674973257,0.,0.65));
#9202=CARTESIAN_POINT('',(0.375277674973257,0.,0.65));
#9203=CARTESIAN_POINT('Origin',(-0.375277674973257,0.,0.65));
#9204=CARTESIAN_POINT('',(-0.375277674973257,0.,0.65));
#9205=CARTESIAN_POINT('',(-0.375277674973257,0.,0.65));
#9206=CARTESIAN_POINT('',(-0.375277674973257,0.,0.65));
#9207=CARTESIAN_POINT('Origin',(-0.750555349946514,0.,-9.19165206894919E-17));
#9208=CARTESIAN_POINT('',(-0.750555349946514,0.,-9.19165206894919E-17));
#9209=CARTESIAN_POINT('',(-0.750555349946514,0.,-9.19165206894919E-17));
#9210=CARTESIAN_POINT('',(-0.750555349946514,0.,-9.19165206894919E-17));
#9211=CARTESIAN_POINT('Origin',(-0.375277674973257,0.,-0.65));
#9212=CARTESIAN_POINT('',(-0.375277674973257,0.,-0.65));
#9213=CARTESIAN_POINT('Origin',(0.,0.53,-1.11022302462516E-16));
#9214=CARTESIAN_POINT('Origin',(0.,0.,-1.11022302462516E-16));
#9584=UNCERTAINTY_MEASURE_WITH_UNIT(LENGTH_MEASURE(0.001),#9623,
'DISTANCE_ACCURACY_VALUE',
'Maximum model space distance between geometric entities at asserted c
onnectivities');
#9592=UNCERTAINTY_MEASURE_WITH_UNIT(LENGTH_MEASURE(0.001),#9623,
'DISTANCE_ACCURACY_VALUE',
'Maximum model space distance between geometric entities at asserted c
onnectivities');
#9614=(
GEOMETRIC_REPRESENTATION_CONTEXT(3)
GLOBAL_UNCERTAINTY_ASSIGNED_CONTEXT((#9584))
GLOBAL_UNIT_ASSIGNED_CONTEXT((#9623,#9625,#9626))
REPRESENTATION_CONTEXT('','3D')
);
#9622=(
GEOMETRIC_REPRESENTATION_CONTEXT(3)
GLOBAL_UNCERTAINTY_ASSIGNED_CONTEXT((#9592))
GLOBAL_UNIT_ASSIGNED_CONTEXT((#9623,#9625,#9626))
REPRESENTATION_CONTEXT('','3D')
);
#9623=(
LENGTH_UNIT()
NAMED_UNIT(*)
SI_UNIT(.CENTI.,.METRE.)
);
#9625=(
NAMED_UNIT(*)
PLANE_ANGLE_UNIT()
SI_UNIT($,.RADIAN.)
);
#9626=(
NAMED_UNIT(*)
SI_UNIT($,.STERADIAN.)
SOLID_ANGLE_UNIT()
);
#9648=SHAPE_DEFINITION_REPRESENTATION(#9682,#9765);
#9682=PRODUCT_DEFINITION_SHAPE('',$,#9795);
#9765=SHAPE_REPRESENTATION('',(#5913),#9614);
#9773=PRODUCT_DEFINITION_CONTEXT('part definition',#9862,'design');
#9795=PRODUCT_DEFINITION('Hex Bolt - M8x40','Hex Bolt - M8x40',#9824,#9773);
#9824=PRODUCT_DEFINITION_FORMATION('',$,#9885);
#9862=APPLICATION_CONTEXT(
'Core Data for Automotive Mechanical Design Process');
#9863=PRODUCT_CONTEXT('part definition',#9862,'mechanical');
#9885=PRODUCT('Hex Bolt - M8x40','Hex Bolt - M8x40','Hex Bolt - M8x40',
(#9863));
#9963=COLOUR_RGB('Black',0.12,0.14,0.17);
#9964=FILL_AREA_STYLE_COLOUR('',#9963);
#9965=FILL_AREA_STYLE('',(#9964));
#9966=SURFACE_STYLE_FILL_AREA(#9965);
#9967=SURFACE_SIDE_STYLE('',(#9966));
#9968=SURFACE_STYLE_USAGE(.BOTH.,#9967);
#9969=PRESENTATION_STYLE_ASSIGNMENT((#9968));
ENDSEC;
END-ISO-10303-21;
